ISO-10303-21;
HEADER;
FILE_DESCRIPTION (('STEP AP203'),
    '1' );
FILE_NAME ('1602p_c_22.step',
    '2026-10-31T14:11:27',
    ( '' ),
    ( '' ),
    'SwSTEP 2.0',
    'SolidWorks 2024',
    '' );
FILE_SCHEMA (( 'AUTOMOTIVE_DESIGN' ));
ENDSEC;

DATA;
#15=CARTESIAN_POINT ( 'NONE',  ( -20.00000000000000000, -20.00000000000000000, 5.000000000004559908 ) ) ;
#81=ORIENTED_EDGE ( 'NONE', *, *, #7510, .T. ) ;
#141=CYLINDRICAL_SURFACE ( 'NONE', #14862, 5.000000000000000888 ) ;
#152=ORIENTED_EDGE ( 'NONE', *, *, #1613, .T. ) ;
#241=EDGE_CURVE ( 'NONE', #7018, #17568, #14626, .T. ) ;
#334=ORIENTED_EDGE ( 'NONE', *, *, #11761, .F. ) ;
#365=DIRECTION ( 'NONE',  ( -8.911056267098788616E-18, -1.998401444326210262E-15, -1.000000000000000000 ) ) ;
#398=CIRCLE ( 'NONE', #17469, 5.000000000000000888 ) ;
#415=DIRECTION ( 'NONE',  ( 1.000000000000000000, 0.000000000000000000, 0.000000000000000000 ) ) ;
#812=EDGE_LOOP ( 'NONE', ( #1100, #19503 ) ) ;
#850=EDGE_CURVE ( 'NONE', #8336, #4807, #22966, .T. ) ;
#853=CARTESIAN_POINT ( 'NONE',  ( -20.00000000000000000, -20.00000000000000000, 5.000000000004559908 ) ) ;
#881=ORIENTED_EDGE ( 'NONE', *, *, #15797, .T. ) ;
#1054=AXIS2_PLACEMENT_3D ( 'NONE', #7400, #18558, #13322 ) ;
#1090=( NAMED_UNIT ( * ) PLANE_ANGLE_UNIT ( ) SI_UNIT ( $, .RADIAN. ) );
#1100=ORIENTED_EDGE ( 'NONE', *, *, #16646, .T. ) ;
#1266=ORIENTED_EDGE ( 'NONE', *, *, #241, .F. ) ;
#1388=SHAPE_REPRESENTATION ( '1602p_c_22', ( #12739 ), #15784 ) ;
#1425=CIRCLE ( 'NONE', #22646, 5.000000000000000888 ) ;
#1543=ORIENTED_EDGE ( 'NONE', *, *, #16093, .F. ) ;
#1581=MANIFOLD_SOLID_BREP ( 'Imported1', #2227 ) ;
#1613=EDGE_CURVE ( 'NONE', #12681, #21263, #15176, .T. ) ;
#1678=CARTESIAN_POINT ( 'NONE',  ( -20.00000000000000000, -22.50000000000000000, 5.500000000004564349 ) ) ;
#1681=DIRECTION ( 'NONE',  ( -8.911056267098788616E-18, -1.998401444326210262E-15, -1.000000000000000000 ) ) ;
#1691=DIRECTION ( 'NONE',  ( 0.000000000000000000, -1.000000000000000000, 1.998401444326210262E-15 ) ) ;
#1693=DIRECTION ( 'NONE',  ( 0.000000000000000000, -1.000000000000000000, 2.081668171172168119E-15 ) ) ;
#1767=DIRECTION ( 'NONE',  ( -8.911056267098788616E-18, -1.998401444326210262E-15, -1.000000000000000000 ) ) ;
#2227=CLOSED_SHELL ( 'NONE', ( #11474, #18289, #19653, #15993, #3459, #2835 ) ) ;
#2569=CARTESIAN_POINT ( 'NONE',  ( 0.000000000000000000, 0.000000000000000000, 0.000000000000000000 ) ) ;
#2824=DIRECTION ( 'NONE',  ( 0.000000000000000000, -1.000000000000000000, 2.081668171172169697E-15 ) ) ;
#2828=SHAPE_DEFINITION_REPRESENTATION ( #6827, #1388 ) ;
#2835=ADVANCED_FACE ( 'NONE', ( #16181, #18330 ), #14176, .T. ) ;
#3228=FACE_OUTER_BOUND ( 'NONE', #22880, .T. ) ;
#3305=VERTEX_POINT ( 'NONE', #16243 ) ;
#3459=ADVANCED_FACE ( 'NONE', ( #6378, #7811 ), #4366, .F. ) ;
#3656=AXIS2_PLACEMENT_3D ( 'NONE', #21414, #5375, #1691 ) ;
#3879=EDGE_LOOP ( 'NONE', ( #334, #20156 ) ) ;
#4103=VERTEX_POINT ( 'NONE', #18941 ) ;
#4279=CARTESIAN_POINT ( 'NONE',  ( -20.00000000000000000, -20.00000000000000000, 5.000000000004559908 ) ) ;
#4303=CIRCLE ( 'NONE', #23240, 2.499999999999998668 ) ;
#4366=PLANE ( 'NONE',  #6106 ) ;
#4470=AXIS2_PLACEMENT_3D ( 'NONE', #17828, #16496, #14255 ) ;
#4535=CARTESIAN_POINT ( 'NONE',  ( -20.00000000000000000, -20.00000000000000000, 5.000000000004559908 ) ) ;
#4625=DIRECTION ( 'NONE',  ( 0.000000000000000000, -1.000000000000000000, 2.081668171172168119E-15 ) ) ;
#4629=EDGE_LOOP ( 'NONE', ( #9506, #15582, #12496, #15235 ) ) ;
#4807=VERTEX_POINT ( 'NONE', #12728 ) ;
#4904=SHAPE_REPRESENTATION_RELATIONSHIP ( 'NONE' , 'NONE' ,  #1388, #10524 ) ;
#4941=DIRECTION ( 'NONE',  ( 0.000000000000000000, -1.000000000000000000, 2.081668171172168119E-15 ) ) ;
#5021=CARTESIAN_POINT ( 'NONE',  ( -20.00000000000000000, -20.00000000000000000, 5.500000000004559020 ) ) ;
#5125=CARTESIAN_POINT ( 'NONE',  ( -19.99999999999999645, -15.00000000000000000, 5.500000000004549250 ) ) ;
#5156=ORIENTED_EDGE ( 'NONE', *, *, #11761, .T. ) ;
#5375=DIRECTION ( 'NONE',  ( -8.911056267098788616E-18, -1.998401444326210262E-15, -1.000000000000000000 ) ) ;
#6106=AXIS2_PLACEMENT_3D ( 'NONE', #11521, #11861, #16943 ) ;
#6190=EDGE_CURVE ( 'NONE', #4103, #3305, #6813, .T. ) ;
#6211=CARTESIAN_POINT ( 'NONE',  ( -20.00000000000000000, -20.00000000000000000, 5.500000000004559020 ) ) ;
#6371=DIRECTION ( 'NONE',  ( -8.911056267098788616E-18, -1.998401444326210262E-15, -1.000000000000000000 ) ) ;
#6376=ORIENTED_EDGE ( 'NONE', *, *, #850, .T. ) ;
#6378=FACE_BOUND ( 'NONE', #19961, .T. ) ;
#6425=AXIS2_PLACEMENT_3D ( 'NONE', #853, #17376, #19616 ) ;
#6554=AXIS2_PLACEMENT_3D ( 'NONE', #6211, #365, #22110 ) ;
#6570=ORIENTED_EDGE ( 'NONE', *, *, #6190, .F. ) ;
#6585=( NAMED_UNIT ( * ) SI_UNIT ( $, .STERADIAN. ) SOLID_ANGLE_UNIT ( ) );
#6813=CIRCLE ( 'NONE', #6425, 2.499999999999998668 ) ;
#6827=PRODUCT_DEFINITION_SHAPE ( 'NONE', 'NONE',  #18531 ) ;
#7018=VERTEX_POINT ( 'NONE', #12368 ) ;
#7400=CARTESIAN_POINT ( 'NONE',  ( -20.00000000000000000, -20.00000000000000000, 5.000000000004559908 ) ) ;
#7510=EDGE_CURVE ( 'NONE', #3305, #21263, #20468, .T. ) ;
#7811=FACE_OUTER_BOUND ( 'NONE', #3879, .T. ) ;
#7931=CYLINDRICAL_SURFACE ( 'NONE', #21685, 2.499999999999998668 ) ;
#8231=EDGE_LOOP ( 'NONE', ( #1266, #20040, #6376, #5156 ) ) ;
#8336=VERTEX_POINT ( 'NONE', #12353 ) ;
#8345=EDGE_LOOP ( 'NONE', ( #10845, #10610 ) ) ;
#9316=CARTESIAN_POINT ( 'NONE',  ( -20.00000000000000000, -22.50000000000000000, 5.000000000004565237 ) ) ;
#9505=DIRECTION ( 'NONE',  ( 8.911056267098788616E-18, 1.998401444326210262E-15, 1.000000000000000000 ) ) ;
#9506=ORIENTED_EDGE ( 'NONE', *, *, #9977, .F. ) ;
#9840=FACE_OUTER_BOUND ( 'NONE', #12805, .T. ) ;
#9977=EDGE_CURVE ( 'NONE', #7018, #8336, #398, .T. ) ;
#10280=LINE ( 'NONE', #12305, #16000 ) ;
#10495=CYLINDRICAL_SURFACE ( 'NONE', #15297, 2.499999999999998668 ) ;
#10524=ADVANCED_BREP_SHAPE_REPRESENTATION ( '', ( #1581, #12739 ), #15784 ) ;
#10610=ORIENTED_EDGE ( 'NONE', *, *, #9977, .T. ) ;
#10637=VECTOR ( 'NONE', #21076, 1000.000000000000000 ) ;
#10845=ORIENTED_EDGE ( 'NONE', *, *, #13013, .T. ) ;
#11425=ORIENTED_EDGE ( 'NONE', *, *, #16093, .T. ) ;
#11474=ADVANCED_FACE ( 'NONE', ( #12829 ), #21732, .T. ) ;
#11521=CARTESIAN_POINT ( 'NONE',  ( -20.00000000000000000, -20.00000000000000000, 5.500000000004559020 ) ) ;
#11525=CARTESIAN_POINT ( 'NONE',  ( -20.00000000000000000, -20.00000000000000000, 5.000000000004559908 ) ) ;
#11761=EDGE_CURVE ( 'NONE', #4807, #17568, #14716, .T. ) ;
#11861=DIRECTION ( 'NONE',  ( -8.911056267098788616E-18, -1.998401444326210262E-15, -1.000000000000000000 ) ) ;
#12026=DIRECTION ( 'NONE',  ( 8.911056267098788616E-18, 1.998401444326210262E-15, 1.000000000000000000 ) ) ;
#12305=CARTESIAN_POINT ( 'NONE',  ( -20.00000000000000000, -17.50000000000000000, 5.000000000004554579 ) ) ;
#12353=CARTESIAN_POINT ( 'NONE',  ( -20.00000000000000000, -25.00000000000000000, 5.000000000004570566 ) ) ;
#12368=CARTESIAN_POINT ( 'NONE',  ( -19.99999999999999645, -15.00000000000000000, 5.000000000004549250 ) ) ;
#12496=ORIENTED_EDGE ( 'NONE', *, *, #13585, .T. ) ;
#12681=VERTEX_POINT ( 'NONE', #17391 ) ;
#12728=CARTESIAN_POINT ( 'NONE',  ( -20.00000000000000000, -25.00000000000000000, 5.500000000004569678 ) ) ;
#12739=AXIS2_PLACEMENT_3D ( 'NONE', #2569, #13380, #415 ) ;
#12750=FACE_OUTER_BOUND ( 'NONE', #8231, .T. ) ;
#12753=UNCERTAINTY_MEASURE_WITH_UNIT (LENGTH_MEASURE( 1.000000000000000082E-05 ), #19172, 'distance_accuracy_value', 'NONE');
#12805=EDGE_LOOP ( 'NONE', ( #6570, #881, #1543, #16263 ) ) ;
#12829=FACE_OUTER_BOUND ( 'NONE', #4629, .T. ) ;
#13013=EDGE_CURVE ( 'NONE', #8336, #7018, #21533, .T. ) ;
#13286=AXIS2_PLACEMENT_3D ( 'NONE', #5021, #1681, #16062 ) ;
#13322=DIRECTION ( 'NONE',  ( 0.000000000000000000, -1.000000000000000000, 2.081668171172168119E-15 ) ) ;
#13380=DIRECTION ( 'NONE',  ( 0.000000000000000000, 0.000000000000000000, 1.000000000000000000 ) ) ;
#13585=EDGE_CURVE ( 'NONE', #17568, #4807, #1425, .T. ) ;
#14088=PRODUCT_DEFINITION_FORMATION_WITH_SPECIFIED_SOURCE ( 'ANY', '', #21034, .NOT_KNOWN. ) ;
#14141=DIRECTION ( 'NONE',  ( 0.000000000000000000, -1.000000000000000000, 2.081668171172168119E-15 ) ) ;
#14176=PLANE ( 'NONE',  #3656 ) ;
#14255=DIRECTION ( 'NONE',  ( 0.000000000000000000, -1.000000000000000000, 2.081668171172168119E-15 ) ) ;
#14626=LINE ( 'NONE', #16740, #16869 ) ;
#14716=CIRCLE ( 'NONE', #20409, 5.000000000000000888 ) ;
#14837=DIRECTION ( 'NONE',  ( 0.000000000000000000, -1.000000000000000000, 2.081668171172169697E-15 ) ) ;
#14862=AXIS2_PLACEMENT_3D ( 'NONE', #15, #23419, #1693 ) ;
#15160=DIRECTION ( 'NONE',  ( 8.911056267098788616E-18, 1.998401444326210262E-15, 1.000000000000000000 ) ) ;
#15176=CIRCLE ( 'NONE', #13286, 2.499999999999998668 ) ;
#15235=ORIENTED_EDGE ( 'NONE', *, *, #850, .F. ) ;
#15297=AXIS2_PLACEMENT_3D ( 'NONE', #4535, #17727, #17263 ) ;
#15348=ORIENTED_EDGE ( 'NONE', *, *, #1613, .F. ) ;
#15582=ORIENTED_EDGE ( 'NONE', *, *, #241, .T. ) ;
#15784=( GEOMETRIC_REPRESENTATION_CONTEXT ( 3 ) GLOBAL_UNCERTAINTY_ASSIGNED_CONTEXT ( ( #12753 ) ) GLOBAL_UNIT_ASSIGNED_CONTEXT ( ( #19172, #1090, #6585 ) ) REPRESENTATION_CONTEXT ( 'NONE', 'WORKASPACE' ) );
#15797=EDGE_CURVE ( 'NONE', #4103, #12681, #10280, .T. ) ;
#15993=ADVANCED_FACE ( 'NONE', ( #12750 ), #141, .T. ) ;
#16000=VECTOR ( 'NONE', #19290, 1000.000000000000000 ) ;
#16062=DIRECTION ( 'NONE',  ( 0.000000000000000000, -1.000000000000000000, 2.081668171172169697E-15 ) ) ;
#16093=EDGE_CURVE ( 'NONE', #21263, #12681, #17163, .T. ) ;
#16181=FACE_BOUND ( 'NONE', #812, .T. ) ;
#16243=CARTESIAN_POINT ( 'NONE',  ( -20.00000000000000000, -22.50000000000000000, 5.000000000004565237 ) ) ;
#16259=APPLICATION_CONTEXT ( 'configuration controlled 3d designs of mechanical parts and assemblies' ) ;
#16263=ORIENTED_EDGE ( 'NONE', *, *, #7510, .F. ) ;
#16302=ORIENTED_EDGE ( 'NONE', *, *, #15797, .F. ) ;
#16400=APPLICATION_CONTEXT ( 'configuration controlled 3d designs of mechanical parts and assemblies' ) ;
#16496=DIRECTION ( 'NONE',  ( 8.911056267098788616E-18, 1.998401444326210262E-15, 1.000000000000000000 ) ) ;
#16570=ORIENTED_EDGE ( 'NONE', *, *, #16646, .F. ) ;
#16646=EDGE_CURVE ( 'NONE', #3305, #4103, #4303, .T. ) ;
#16740=CARTESIAN_POINT ( 'NONE',  ( -19.99999999999999645, -15.00000000000000000, 5.000000000004549250 ) ) ;
#16869=VECTOR ( 'NONE', #18072, 1000.000000000000000 ) ;
#16943=DIRECTION ( 'NONE',  ( 0.000000000000000000, -1.000000000000000000, 1.998401444326210262E-15 ) ) ;
#17163=CIRCLE ( 'NONE', #6554, 2.499999999999998668 ) ;
#17199=VECTOR ( 'NONE', #12026, 1000.000000000000000 ) ;
#17228=CARTESIAN_POINT ( 'NONE',  ( -20.00000000000000000, -20.00000000000000000, 5.500000000004559020 ) ) ;
#17263=DIRECTION ( 'NONE',  ( 0.000000000000000000, -1.000000000000000000, 2.081668171172169697E-15 ) ) ;
#17376=DIRECTION ( 'NONE',  ( 8.911056267098788616E-18, 1.998401444326210262E-15, 1.000000000000000000 ) ) ;
#17391=CARTESIAN_POINT ( 'NONE',  ( -20.00000000000000000, -17.50000000000000000, 5.500000000004554579 ) ) ;
#17469=AXIS2_PLACEMENT_3D ( 'NONE', #21385, #1767, #14141 ) ;
#17568=VERTEX_POINT ( 'NONE', #5125 ) ;
#17577=DIRECTION ( 'NONE',  ( -8.911056267098788616E-18, -1.998401444326210262E-15, -1.000000000000000000 ) ) ;
#17727=DIRECTION ( 'NONE',  ( 8.911056267098788616E-18, 1.998401444326210262E-15, 1.000000000000000000 ) ) ;
#17828=CARTESIAN_POINT ( 'NONE',  ( -20.00000000000000000, -20.00000000000000000, 5.000000000004559908 ) ) ;
#18072=DIRECTION ( 'NONE',  ( 8.911056267098788616E-18, 1.998401444326210262E-15, 1.000000000000000000 ) ) ;
#18289=ADVANCED_FACE ( 'NONE', ( #9840 ), #7931, .F. ) ;
#18330=FACE_OUTER_BOUND ( 'NONE', #8345, .T. ) ;
#18531=PRODUCT_DEFINITION ( 'UNKNOWN', '', #14088, #19902 ) ;
#18558=DIRECTION ( 'NONE',  ( -8.911056267098788616E-18, -1.998401444326210262E-15, -1.000000000000000000 ) ) ;
#18941=CARTESIAN_POINT ( 'NONE',  ( -20.00000000000000000, -17.50000000000000000, 5.000000000004554579 ) ) ;
#18966=CARTESIAN_POINT ( 'NONE',  ( -20.00000000000000000, -20.00000000000000000, 5.500000000004559020 ) ) ;
#19172=( LENGTH_UNIT ( ) NAMED_UNIT ( * ) SI_UNIT ( .MILLI., .METRE. ) );
#19290=DIRECTION ( 'NONE',  ( 8.911056267098788616E-18, 1.998401444326210262E-15, 1.000000000000000000 ) ) ;
#19503=ORIENTED_EDGE ( 'NONE', *, *, #6190, .T. ) ;
#19616=DIRECTION ( 'NONE',  ( 0.000000000000000000, -1.000000000000000000, 2.081668171172169697E-15 ) ) ;
#19653=ADVANCED_FACE ( 'NONE', ( #3228 ), #10495, .F. ) ;
#19902=DESIGN_CONTEXT ( 'detailed design', #16259, 'design' ) ;
#19961=EDGE_LOOP ( 'NONE', ( #11425, #152 ) ) ;
#20040=ORIENTED_EDGE ( 'NONE', *, *, #13013, .F. ) ;
#20156=ORIENTED_EDGE ( 'NONE', *, *, #13585, .F. ) ;
#20409=AXIS2_PLACEMENT_3D ( 'NONE', #17228, #17577, #4625 ) ;
#20468=LINE ( 'NONE', #9316, #17199 ) ;
#21034=PRODUCT ( '1602p_c_22', '1602p_c_22', '', ( #22756 ) ) ;
#21076=DIRECTION ( 'NONE',  ( 8.911056267098788616E-18, 1.998401444326210262E-15, 1.000000000000000000 ) ) ;
#21263=VERTEX_POINT ( 'NONE', #1678 ) ;
#21385=CARTESIAN_POINT ( 'NONE',  ( -20.00000000000000000, -20.00000000000000000, 5.000000000004559908 ) ) ;
#21414=CARTESIAN_POINT ( 'NONE',  ( -20.00000000000000000, -20.00000000000000000, 5.000000000004559908 ) ) ;
#21533=CIRCLE ( 'NONE', #1054, 5.000000000000000888 ) ;
#21685=AXIS2_PLACEMENT_3D ( 'NONE', #11525, #15160, #2824 ) ;
#21732=CYLINDRICAL_SURFACE ( 'NONE', #4470, 5.000000000000000888 ) ;
#22110=DIRECTION ( 'NONE',  ( 0.000000000000000000, -1.000000000000000000, 2.081668171172169697E-15 ) ) ;
#22509=CARTESIAN_POINT ( 'NONE',  ( -20.00000000000000000, -25.00000000000000000, 5.000000000004570566 ) ) ;
#22646=AXIS2_PLACEMENT_3D ( 'NONE', #18966, #6371, #4941 ) ;
#22756=MECHANICAL_CONTEXT ( 'NONE', #16400, 'mechanical' ) ;
#22880=EDGE_LOOP ( 'NONE', ( #16302, #16570, #81, #15348 ) ) ;
#22966=LINE ( 'NONE', #22509, #10637 ) ;
#23240=AXIS2_PLACEMENT_3D ( 'NONE', #4279, #9505, #14837 ) ;
#23419=DIRECTION ( 'NONE',  ( 8.911056267098788616E-18, 1.998401444326210262E-15, 1.000000000000000000 ) ) ;
#23550=COLOUR_RGB('Black', 0.08235294, 0.09019608, 0.10196078);
#23551=FILL_AREA_STYLE_COLOUR('',#23550);
#23552=FILL_AREA_STYLE('',(#23551));
#23553=SURFACE_STYLE_FILL_AREA(#23552);
#23554=SURFACE_SIDE_STYLE('',(#23553));
#23555=SURFACE_STYLE_USAGE(.BOTH.,#23554);
#23556=PRESENTATION_STYLE_ASSIGNMENT((#23555));
#23583=STYLED_ITEM('',(#23556),#1581);
#23584=MECHANICAL_DESIGN_GEOMETRIC_PRESENTATION_REPRESENTATION('',(#23583),#15784);
ENDSEC;
END-ISO-10303-21;
